ISO-10303-21;
HEADER;
/* Generated by software containing ST-Developer
 * from STEP Tools, Inc. (www.steptools.com) 
 */

FILE_DESCRIPTION(
/* description */ ('Cylinder foot and clevis mount kit'),
/* implementation_level */ '2;1');

FILE_NAME(
/* name */ 'Clevis Pin - 6x30.step',
/* time_stamp */ '2026-10-27T20:10:43-07:00',
/* author */ (''),
/* organization */ (''),
/* preprocessor_version */ 'ST-DEVELOPER v20.2',
/* originating_system */ 'Autodesk Translation Framework v15.17.0.0',
/* authorisation */ '');

FILE_SCHEMA (('AUTOMOTIVE_DESIGN { 1 0 10303 214 3 1 1 }'));
ENDSEC;

DATA;
#10=MECHANICAL_DESIGN_GEOMETRIC_PRESENTATION_REPRESENTATION('',(#363),#9102);
#13=B_SPLINE_CURVE_WITH_KNOTS('',3,(#8834,#8835,#8836,#8837,#8838,#8839,
#8840,#8841,#8842,#8843),.UNSPECIFIED.,.F.,.F.,(4,2,2,2,4),(0.,0.0302963256060356,
0.0605926512120712,0.090883446720838,0.121174242229605),.UNSPECIFIED.);
#14=B_SPLINE_CURVE_WITH_KNOTS('',3,(#8846,#8847,#8848,#8849,#8850,#8851,
#8852,#8853,#8854,#8855,#8856,#8857,#8858,#8859,#8860,#8861,#8862,#8863,
#8864,#8865,#8866,#8867,#8868,#8869,#8870,#8871,#8872,#8873,#8874,#8875,
#8876,#8877,#8878,#8879),.UNSPECIFIED.,.T.,.F.,(4,2,2,2,2,2,2,2,2,2,2,2,
2,2,2,2,4),(0.,0.0302963256060358,0.0605926512120716,0.0908834467208383,
0.121174242229605,0.151465037738372,0.181755833247138,0.212052158853174,
0.24234848445921,0.272644810065246,0.302941135671282,0.333231931180048,
0.363522726688815,0.393813522197582,0.424104317706349,0.454400643312384,
0.48469696891842),.UNSPECIFIED.);
#15=B_SPLINE_CURVE_WITH_KNOTS('',3,(#8881,#8882,#8883,#8884,#8885,#8886,
#8887,#8888,#8889,#8890),.UNSPECIFIED.,.F.,.F.,(4,2,2,2,4),(0.363522726688815,
0.393813522197581,0.424104317706348,0.454400643312384,0.48469696891842),
 .UNSPECIFIED.);
#16=B_SPLINE_CURVE_WITH_KNOTS('',3,(#8891,#8892,#8893,#8894,#8895,#8896,
#8897,#8898,#8899,#8900,#8901,#8902,#8903,#8904,#8905,#8906,#8907,#8908),
 .UNSPECIFIED.,.F.,.F.,(4,2,2,2,2,2,2,2,4),(0.121174242229605,0.151465037738371,
0.181755833247138,0.212052158853174,0.24234848445921,0.272644810065246,
0.302941135671281,0.333231931180048,0.363522726688815),.UNSPECIFIED.);
#280=CONICAL_SURFACE('',#5847,0.475,0.785398163397448);
#281=CONICAL_SURFACE('',#5855,0.255,0.785398163397449);
#307=SHAPE_REPRESENTATION_RELATIONSHIP('SRR','None',#9256,#335);
#335=ADVANCED_BREP_SHAPE_REPRESENTATION('',(#389),#9099);
#363=STYLED_ITEM('',(#9460),#389);
#389=MANIFOLD_SOLID_BREP('Body1',#4951);
#490=FACE_BOUND('',#1393,.T.);
#491=FACE_BOUND('',#1395,.T.);
#687=PLANE('',#5845);
#688=PLANE('',#5851);
#689=PLANE('',#5857);
#984=FACE_OUTER_BOUND('',#1388,.T.);
#985=FACE_OUTER_BOUND('',#1389,.T.);
#986=FACE_OUTER_BOUND('',#1390,.T.);
#987=FACE_OUTER_BOUND('',#1391,.T.);
#988=FACE_OUTER_BOUND('',#1392,.T.);
#989=FACE_OUTER_BOUND('',#1394,.T.);
#990=FACE_OUTER_BOUND('',#1396,.T.);
#991=FACE_OUTER_BOUND('',#1397,.T.);
#1388=EDGE_LOOP('',(#4453,#4454,#4455,#4456,#4457,#4458));
#1389=EDGE_LOOP('',(#4459));
#1390=EDGE_LOOP('',(#4460,#4461,#4462,#4463));
#1391=EDGE_LOOP('',(#4464,#4465,#4466,#4467));
#1392=EDGE_LOOP('',(#4468));
#1393=EDGE_LOOP('',(#4469));
#1394=EDGE_LOOP('',(#4470,#4471,#4472,#4473,#4474,#4475,#4476,#4477,#4478));
#1395=EDGE_LOOP('',(#4479));
#1396=EDGE_LOOP('',(#4480,#4481,#4482,#4483));
#1397=EDGE_LOOP('',(#4484));
#1746=LINE('',#8845,#2095);
#1747=LINE('',#8915,#2096);
#1748=LINE('',#8919,#2097);
#1749=LINE('',#8926,#2098);
#1750=LINE('',#8927,#2099);
#1751=LINE('',#8931,#2100);
#2095=VECTOR('',#7391,0.08);
#2096=VECTOR('',#7400,0.475);
#2097=VECTOR('',#7405,0.5);
#2098=VECTOR('',#7414,0.3);
#2099=VECTOR('',#7415,0.3);
#2100=VECTOR('',#7420,0.255);
#2313=CIRCLE('',#5846,0.45);
#2314=CIRCLE('',#5848,0.5);
#2315=CIRCLE('',#5850,0.5);
#2316=CIRCLE('',#5852,0.3);
#2317=CIRCLE('',#5854,0.3);
#2318=CIRCLE('',#5856,0.21);
#2690=VERTEX_POINT('',#8832);
#2691=VERTEX_POINT('',#8833);
#2692=VERTEX_POINT('',#8844);
#2693=VERTEX_POINT('',#8880);
#2694=VERTEX_POINT('',#8910);
#2695=VERTEX_POINT('',#8913);
#2696=VERTEX_POINT('',#8917);
#2697=VERTEX_POINT('',#8921);
#2698=VERTEX_POINT('',#8924);
#2699=VERTEX_POINT('',#8929);
#3281=EDGE_CURVE('',#2690,#2691,#13,.T.);
#3282=EDGE_CURVE('',#2690,#2692,#1746,.T.);
#3283=EDGE_CURVE('',#2692,#2692,#14,.T.);
#3284=EDGE_CURVE('',#2693,#2690,#15,.T.);
#3285=EDGE_CURVE('',#2691,#2693,#16,.T.);
#3286=EDGE_CURVE('',#2694,#2694,#2313,.T.);
#3287=EDGE_CURVE('',#2695,#2695,#2314,.T.);
#3288=EDGE_CURVE('',#2695,#2694,#1747,.T.);
#3289=EDGE_CURVE('',#2696,#2696,#2315,.T.);
#3290=EDGE_CURVE('',#2696,#2695,#1748,.T.);
#3291=EDGE_CURVE('',#2697,#2697,#2316,.T.);
#3292=EDGE_CURVE('',#2698,#2698,#2317,.T.);
#3293=EDGE_CURVE('',#2698,#2691,#1749,.T.);
#3294=EDGE_CURVE('',#2693,#2697,#1750,.T.);
#3295=EDGE_CURVE('',#2699,#2699,#2318,.T.);
#3296=EDGE_CURVE('',#2699,#2698,#1751,.T.);
#4453=ORIENTED_EDGE('',*,*,#3281,.F.);
#4454=ORIENTED_EDGE('',*,*,#3282,.T.);
#4455=ORIENTED_EDGE('',*,*,#3283,.F.);
#4456=ORIENTED_EDGE('',*,*,#3282,.F.);
#4457=ORIENTED_EDGE('',*,*,#3284,.F.);
#4458=ORIENTED_EDGE('',*,*,#3285,.F.);
#4459=ORIENTED_EDGE('',*,*,#3286,.F.);
#4460=ORIENTED_EDGE('',*,*,#3287,.F.);
#4461=ORIENTED_EDGE('',*,*,#3288,.T.);
#4462=ORIENTED_EDGE('',*,*,#3286,.T.);
#4463=ORIENTED_EDGE('',*,*,#3288,.F.);
#4464=ORIENTED_EDGE('',*,*,#3289,.F.);
#4465=ORIENTED_EDGE('',*,*,#3290,.T.);
#4466=ORIENTED_EDGE('',*,*,#3287,.T.);
#4467=ORIENTED_EDGE('',*,*,#3290,.F.);
#4468=ORIENTED_EDGE('',*,*,#3289,.T.);
#4469=ORIENTED_EDGE('',*,*,#3291,.F.);
#4470=ORIENTED_EDGE('',*,*,#3292,.F.);
#4471=ORIENTED_EDGE('',*,*,#3293,.T.);
#4472=ORIENTED_EDGE('',*,*,#3285,.T.);
#4473=ORIENTED_EDGE('',*,*,#3294,.T.);
#4474=ORIENTED_EDGE('',*,*,#3291,.T.);
#4475=ORIENTED_EDGE('',*,*,#3294,.F.);
#4476=ORIENTED_EDGE('',*,*,#3284,.T.);
#4477=ORIENTED_EDGE('',*,*,#3281,.T.);
#4478=ORIENTED_EDGE('',*,*,#3293,.F.);
#4479=ORIENTED_EDGE('',*,*,#3283,.T.);
#4480=ORIENTED_EDGE('',*,*,#3295,.F.);
#4481=ORIENTED_EDGE('',*,*,#3296,.T.);
#4482=ORIENTED_EDGE('',*,*,#3292,.T.);
#4483=ORIENTED_EDGE('',*,*,#3296,.F.);
#4484=ORIENTED_EDGE('',*,*,#3295,.T.);
#4612=CYLINDRICAL_SURFACE('',#5844,0.08);
#4613=CYLINDRICAL_SURFACE('',#5849,0.5);
#4614=CYLINDRICAL_SURFACE('',#5853,0.3);
#4907=ADVANCED_FACE('',(#984),#4612,.F.);
#4908=ADVANCED_FACE('',(#985),#687,.T.);
#4909=ADVANCED_FACE('',(#986),#280,.T.);
#4910=ADVANCED_FACE('',(#987),#4613,.T.);
#4911=ADVANCED_FACE('',(#988,#490),#688,.T.);
#4912=ADVANCED_FACE('',(#989,#491),#4614,.T.);
#4913=ADVANCED_FACE('',(#990),#281,.T.);
#4914=ADVANCED_FACE('',(#991),#689,.T.);
#4951=CLOSED_SHELL('',(#4907,#4908,#4909,#4910,#4911,#4912,#4913,#4914));
#5843=AXIS2_PLACEMENT_3D('',#8830,#7387,#7388);
#5844=AXIS2_PLACEMENT_3D('',#8831,#7389,#7390);
#5845=AXIS2_PLACEMENT_3D('',#8909,#7392,#7393);
#5846=AXIS2_PLACEMENT_3D('',#8911,#7394,#7395);
#5847=AXIS2_PLACEMENT_3D('',#8912,#7396,#7397);
#5848=AXIS2_PLACEMENT_3D('',#8914,#7398,#7399);
#5849=AXIS2_PLACEMENT_3D('',#8916,#7401,#7402);
#5850=AXIS2_PLACEMENT_3D('',#8918,#7403,#7404);
#5851=AXIS2_PLACEMENT_3D('',#8920,#7406,#7407);
#5852=AXIS2_PLACEMENT_3D('',#8922,#7408,#7409);
#5853=AXIS2_PLACEMENT_3D('',#8923,#7410,#7411);
#5854=AXIS2_PLACEMENT_3D('',#8925,#7412,#7413);
#5855=AXIS2_PLACEMENT_3D('',#8928,#7416,#7417);
#5856=AXIS2_PLACEMENT_3D('',#8930,#7418,#7419);
#5857=AXIS2_PLACEMENT_3D('',#8932,#7421,#7422);
#7387=DIRECTION('axis',(0.,0.,1.));
#7388=DIRECTION('refdir',(1.,0.,0.));
#7389=DIRECTION('center_axis',(1.,0.,0.));
#7390=DIRECTION('ref_axis',(0.,0.,-1.));
#7391=DIRECTION('',(1.,0.,0.));
#7392=DIRECTION('center_axis',(0.,1.,0.));
#7393=DIRECTION('ref_axis',(0.,0.,1.));
#7394=DIRECTION('center_axis',(0.,-1.,0.));
#7395=DIRECTION('ref_axis',(1.,0.,0.));
#7396=DIRECTION('center_axis',(0.,-1.,0.));
#7397=DIRECTION('ref_axis',(1.,0.,0.));
#7398=DIRECTION('center_axis',(0.,-1.,0.));
#7399=DIRECTION('ref_axis',(1.,0.,0.));
#7400=DIRECTION('',(0.707106781186547,0.707106781186548,8.65956056235493E-17));
#7401=DIRECTION('center_axis',(0.,-1.,0.));
#7402=DIRECTION('ref_axis',(1.,0.,0.));
#7403=DIRECTION('center_axis',(0.,-1.,0.));
#7404=DIRECTION('ref_axis',(1.,0.,0.));
#7405=DIRECTION('',(0.,1.,0.));
#7406=DIRECTION('center_axis',(0.,-1.,0.));
#7407=DIRECTION('ref_axis',(0.,0.,-1.));
#7408=DIRECTION('center_axis',(0.,-1.,0.));
#7409=DIRECTION('ref_axis',(1.,0.,0.));
#7410=DIRECTION('center_axis',(0.,-1.,0.));
#7411=DIRECTION('ref_axis',(1.,0.,0.));
#7412=DIRECTION('center_axis',(0.,-1.,0.));
#7413=DIRECTION('ref_axis',(1.,0.,0.));
#7414=DIRECTION('',(0.,1.,0.));
#7415=DIRECTION('',(0.,1.,0.));
#7416=DIRECTION('center_axis',(0.,1.,0.));
#7417=DIRECTION('ref_axis',(1.,0.,0.));
#7418=DIRECTION('center_axis',(0.,-1.,0.));
#7419=DIRECTION('ref_axis',(1.,0.,0.));
#7420=DIRECTION('',(-0.707106781186548,0.707106781186547,-8.65956056235494E-17));
#7421=DIRECTION('center_axis',(0.,-1.,0.));
#7422=DIRECTION('ref_axis',(0.,0.,-1.));
#8830=CARTESIAN_POINT('',(0.,0.,0.));
#8831=CARTESIAN_POINT('Origin',(0.,-2.7,0.));
#8832=CARTESIAN_POINT('',(-0.289136645896019,-2.7,0.08));
#8833=CARTESIAN_POINT('',(-0.3,-2.78,-2.27065106771523E-17));
#8834=CARTESIAN_POINT('Ctrl Pts',(-0.289136645896019,-2.7,0.08));
#8835=CARTESIAN_POINT('Ctrl Pts',(-0.289136645896019,-2.71009877520201,
0.08));
#8836=CARTESIAN_POINT('Ctrl Pts',(-0.289720927595908,-2.72083518625944,
0.0779717130936404));
#8837=CARTESIAN_POINT('Ctrl Pts',(-0.291799203044223,-2.74052980652726,
0.0697927537456149));
#8838=CARTESIAN_POINT('Ctrl Pts',(-0.293259762986909,-2.74949254880105,
0.0636445361887959));
#8839=CARTESIAN_POINT('Ctrl Pts',(-0.295976783522942,-2.76364324458222,
0.0494938404076284));
#8840=CARTESIAN_POINT('Ctrl Pts',(-0.297414335384467,-2.76979246713824,
0.0405305642602551));
#8841=CARTESIAN_POINT('Ctrl Pts',(-0.299439403644655,-2.77797216257078,
0.0208340363410407));
#8842=CARTESIAN_POINT('Ctrl Pts',(-0.3,-2.78,0.0100969318362556));
#8843=CARTESIAN_POINT('Ctrl Pts',(-0.3,-2.78,5.20417042793042E-18));
#8844=CARTESIAN_POINT('',(0.289136645896019,-2.7,0.08));
#8845=CARTESIAN_POINT('',(0.,-2.7,0.08));
#8846=CARTESIAN_POINT('Ctrl Pts',(0.289136645896019,-2.7,0.08));
#8847=CARTESIAN_POINT('Ctrl Pts',(0.289136645896019,-2.68990122479799,0.08));
#8848=CARTESIAN_POINT('Ctrl Pts',(0.289720927595908,-2.67916481374056,0.0779717130936404));
#8849=CARTESIAN_POINT('Ctrl Pts',(0.291799203044223,-2.65947019347274,0.0697927537456147));
#8850=CARTESIAN_POINT('Ctrl Pts',(0.293259762986909,-2.65050745119895,0.0636445361887959));
#8851=CARTESIAN_POINT('Ctrl Pts',(0.295976783522942,-2.63635675541778,0.0494938404076283));
#8852=CARTESIAN_POINT('Ctrl Pts',(0.297414335384467,-2.63020753286176,0.0405305642602551));
#8853=CARTESIAN_POINT('Ctrl Pts',(0.299439403644655,-2.62202783742922,0.0208340363410406));
#8854=CARTESIAN_POINT('Ctrl Pts',(0.3,-2.62,0.0100969318362555));
#8855=CARTESIAN_POINT('Ctrl Pts',(0.3,-2.62,-0.0100969318362556));
#8856=CARTESIAN_POINT('Ctrl Pts',(0.299439403644655,-2.62202783742922,-0.0208340363410406));
#8857=CARTESIAN_POINT('Ctrl Pts',(0.297414335384467,-2.63020753286176,-0.0405305642602551));
#8858=CARTESIAN_POINT('Ctrl Pts',(0.295976783522942,-2.63635675541778,-0.0494938404076283));
#8859=CARTESIAN_POINT('Ctrl Pts',(0.293259762986909,-2.65050745119895,-0.0636445361887959));
#8860=CARTESIAN_POINT('Ctrl Pts',(0.291799203044223,-2.65947019347274,-0.0697927537456147));
#8861=CARTESIAN_POINT('Ctrl Pts',(0.289720927595908,-2.67916481374056,-0.0779717130936403));
#8862=CARTESIAN_POINT('Ctrl Pts',(0.289136645896019,-2.68990122479799,-0.08));
#8863=CARTESIAN_POINT('Ctrl Pts',(0.289136645896019,-2.71009877520201,-0.08));
#8864=CARTESIAN_POINT('Ctrl Pts',(0.289720927595908,-2.72083518625944,-0.0779717130936404));
#8865=CARTESIAN_POINT('Ctrl Pts',(0.291799203044223,-2.74052980652726,-0.0697927537456147));
#8866=CARTESIAN_POINT('Ctrl Pts',(0.293259762986909,-2.74949254880105,-0.0636445361887959));
#8867=CARTESIAN_POINT('Ctrl Pts',(0.295976783522942,-2.76364324458222,-0.0494938404076283));
#8868=CARTESIAN_POINT('Ctrl Pts',(0.297414335384467,-2.76979246713824,-0.0405305642602551));
#8869=CARTESIAN_POINT('Ctrl Pts',(0.299439403644655,-2.77797216257078,-0.0208340363410406));
#8870=CARTESIAN_POINT('Ctrl Pts',(0.3,-2.78,-0.0100969318362555));
#8871=CARTESIAN_POINT('Ctrl Pts',(0.3,-2.78,0.0100969318362556));
#8872=CARTESIAN_POINT('Ctrl Pts',(0.299439403644655,-2.77797216257078,0.0208340363410407));
#8873=CARTESIAN_POINT('Ctrl Pts',(0.297414335384467,-2.76979246713824,0.0405305642602551));
#8874=CARTESIAN_POINT('Ctrl Pts',(0.295976783522942,-2.76364324458222,0.0494938404076284));
#8875=CARTESIAN_POINT('Ctrl Pts',(0.293259762986909,-2.74949254880105,0.0636445361887959));
#8876=CARTESIAN_POINT('Ctrl Pts',(0.291799203044223,-2.74052980652726,0.0697927537456149));
#8877=CARTESIAN_POINT('Ctrl Pts',(0.289720927595908,-2.72083518625944,0.0779717130936404));
#8878=CARTESIAN_POINT('Ctrl Pts',(0.289136645896019,-2.71009877520201,0.08));
#8879=CARTESIAN_POINT('Ctrl Pts',(0.289136645896019,-2.7,0.08));
#8880=CARTESIAN_POINT('',(-0.3,-2.62,-3.65842984849668E-17));
#8881=CARTESIAN_POINT('Ctrl Pts',(-0.3,-2.62,-3.81639164714898E-17));
#8882=CARTESIAN_POINT('Ctrl Pts',(-0.3,-2.62,0.0100969318362555));
#8883=CARTESIAN_POINT('Ctrl Pts',(-0.299439403644655,-2.62202783742922,
0.0208340363410406));
#8884=CARTESIAN_POINT('Ctrl Pts',(-0.297414335384467,-2.63020753286176,
0.040530564260255));
#8885=CARTESIAN_POINT('Ctrl Pts',(-0.295976783522942,-2.63635675541778,
0.0494938404076283));
#8886=CARTESIAN_POINT('Ctrl Pts',(-0.293259762986909,-2.65050745119895,
0.0636445361887959));
#8887=CARTESIAN_POINT('Ctrl Pts',(-0.291799203044223,-2.65947019347274,
0.0697927537456147));
#8888=CARTESIAN_POINT('Ctrl Pts',(-0.289720927595908,-2.67916481374056,
0.0779717130936404));
#8889=CARTESIAN_POINT('Ctrl Pts',(-0.289136645896019,-2.68990122479799,
0.08));
#8890=CARTESIAN_POINT('Ctrl Pts',(-0.289136645896019,-2.7,0.08));
#8891=CARTESIAN_POINT('Ctrl Pts',(-0.3,-2.78,-6.93889390390723E-18));
#8892=CARTESIAN_POINT('Ctrl Pts',(-0.3,-2.78,-0.0100969318362556));
#8893=CARTESIAN_POINT('Ctrl Pts',(-0.299439403644655,-2.77797216257078,
-0.0208340363410406));
#8894=CARTESIAN_POINT('Ctrl Pts',(-0.297414335384467,-2.76979246713824,
-0.0405305642602551));
#8895=CARTESIAN_POINT('Ctrl Pts',(-0.295976783522942,-2.76364324458222,
-0.0494938404076283));
#8896=CARTESIAN_POINT('Ctrl Pts',(-0.293259762986909,-2.74949254880105,
-0.0636445361887959));
#8897=CARTESIAN_POINT('Ctrl Pts',(-0.291799203044223,-2.74052980652726,
-0.0697927537456147));
#8898=CARTESIAN_POINT('Ctrl Pts',(-0.289720927595908,-2.72083518625944,
-0.0779717130936403));
#8899=CARTESIAN_POINT('Ctrl Pts',(-0.289136645896019,-2.71009877520201,
-0.08));
#8900=CARTESIAN_POINT('Ctrl Pts',(-0.289136645896019,-2.68990122479799,
-0.08));
#8901=CARTESIAN_POINT('Ctrl Pts',(-0.289720927595908,-2.67916481374056,
-0.0779717130936403));
#8902=CARTESIAN_POINT('Ctrl Pts',(-0.291799203044223,-2.65947019347274,
-0.0697927537456147));
#8903=CARTESIAN_POINT('Ctrl Pts',(-0.293259762986909,-2.65050745119895,
-0.0636445361887959));
#8904=CARTESIAN_POINT('Ctrl Pts',(-0.295976783522942,-2.63635675541778,
-0.0494938404076283));
#8905=CARTESIAN_POINT('Ctrl Pts',(-0.297414335384467,-2.63020753286176,
-0.0405305642602551));
#8906=CARTESIAN_POINT('Ctrl Pts',(-0.299439403644655,-2.62202783742922,
-0.0208340363410406));
#8907=CARTESIAN_POINT('Ctrl Pts',(-0.3,-2.62,-0.0100969318362556));
#8908=CARTESIAN_POINT('Ctrl Pts',(-0.3,-2.62,-1.56125112837913E-17));
#8909=CARTESIAN_POINT('Origin',(0.45,0.2,0.));
#8910=CARTESIAN_POINT('',(-0.45,0.2,-5.51091059616309E-17));
#8911=CARTESIAN_POINT('Origin',(0.,0.2,0.));
#8912=CARTESIAN_POINT('Origin',(0.,0.175,0.));
#8913=CARTESIAN_POINT('',(-0.5,0.15,-6.12323399573676E-17));
#8914=CARTESIAN_POINT('Origin',(0.,0.15,0.));
#8915=CARTESIAN_POINT('',(-0.475,0.175,-5.81707229594993E-17));
#8916=CARTESIAN_POINT('Origin',(0.,0.0750000000000002,0.));
#8917=CARTESIAN_POINT('',(-0.5,0.,-6.12323399573677E-17));
#8918=CARTESIAN_POINT('Origin',(0.,0.,0.));
#8919=CARTESIAN_POINT('',(-0.5,0.0750000000000002,-6.12323399573677E-17));
#8920=CARTESIAN_POINT('Origin',(0.3,0.,0.));
#8921=CARTESIAN_POINT('',(-0.3,0.,-3.67394039744206E-17));
#8922=CARTESIAN_POINT('Origin',(0.,0.,0.));
#8923=CARTESIAN_POINT('Origin',(0.,-1.455,0.));
#8924=CARTESIAN_POINT('',(-0.3,-2.91,-3.67394039744206E-17));
#8925=CARTESIAN_POINT('Origin',(0.,-2.91,0.));
#8926=CARTESIAN_POINT('',(-0.3,-1.455,-3.67394039744206E-17));
#8927=CARTESIAN_POINT('',(-0.3,-1.455,-3.67394039744206E-17));
#8928=CARTESIAN_POINT('Origin',(0.,-2.955,0.));
#8929=CARTESIAN_POINT('',(-0.21,-3.,-2.57175827820944E-17));
#8930=CARTESIAN_POINT('Origin',(0.,-3.,0.));
#8931=CARTESIAN_POINT('',(-0.255,-2.955,-3.12284933782575E-17));
#8932=CARTESIAN_POINT('Origin',(0.,-3.,0.));
#9066=UNCERTAINTY_MEASURE_WITH_UNIT(LENGTH_MEASURE(0.001),#9103,
'DISTANCE_ACCURACY_VALUE',
'Maximum model space distance between geometric entities at asserted c
onnectivities');
#9069=UNCERTAINTY_MEASURE_WITH_UNIT(LENGTH_MEASURE(0.001),#9103,
'DISTANCE_ACCURACY_VALUE',
'Maximum model space distance between geometric entities at asserted c
onnectivities');
#9099=(
GEOMETRIC_REPRESENTATION_CONTEXT(3)
GLOBAL_UNCERTAINTY_ASSIGNED_CONTEXT((#9066))
GLOBAL_UNIT_ASSIGNED_CONTEXT((#9103,#9105,#9106))
REPRESENTATION_CONTEXT('','3D')
);
#9102=(
GEOMETRIC_REPRESENTATION_CONTEXT(3)
GLOBAL_UNCERTAINTY_ASSIGNED_CONTEXT((#9069))
GLOBAL_UNIT_ASSIGNED_CONTEXT((#9103,#9105,#9106))
REPRESENTATION_CONTEXT('','3D')
);
#9103=(
LENGTH_UNIT()
NAMED_UNIT(*)
SI_UNIT(.CENTI.,.METRE.)
);
#9105=(
NAMED_UNIT(*)
PLANE_ANGLE_UNIT()
SI_UNIT($,.RADIAN.)
);
#9106=(
NAMED_UNIT(*)
SI_UNIT($,.STERADIAN.)
SOLID_ANGLE_UNIT()
);
#9136=SHAPE_DEFINITION_REPRESENTATION(#9211,#9256);
#9211=PRODUCT_DEFINITION_SHAPE('',$,#9289);
#9256=SHAPE_REPRESENTATION('',(#5843),#9099);
#9259=PRODUCT_DEFINITION_CONTEXT('part definition',#9357,'design');
#9289=PRODUCT_DEFINITION('Clevis Pin - 6x30','Clevis Pin - 6x30',#9321,
#9259);
#9321=PRODUCT_DEFINITION_FORMATION('',$,#9388);
#9357=APPLICATION_CONTEXT(
'Core Data for Automotive Mechanical Design Process');
#9358=PRODUCT_CONTEXT('part definition',#9357,'mechanical');
#9388=PRODUCT('Clevis Pin - 6x30','Clevis Pin - 6x30',
'Clevis Pin - 6x30',(#9358));
#9454=COLOUR_RGB('Grey',0.48,0.52,0.57);
#9455=FILL_AREA_STYLE_COLOUR('',#9454);
#9456=FILL_AREA_STYLE('',(#9455));
#9457=SURFACE_STYLE_FILL_AREA(#9456);
#9458=SURFACE_SIDE_STYLE('',(#9457));
#9459=SURFACE_STYLE_USAGE(.BOTH.,#9458);
#9460=PRESENTATION_STYLE_ASSIGNMENT((#9459));
ENDSEC;
END-ISO-10303-21;
